ISO-10303-21;
HEADER;
/* Generated by software containing ST-Developer
 * from STEP Tools, Inc. (www.steptools.com) 
 */

FILE_DESCRIPTION(
/* description */ ('Bin tilter linkage'),
/* implementation_level */ '2;1');

FILE_NAME(
/* name */ 'Pivot keeper (3).step',
/* time_stamp */ '2026-10-28T03:26:24-07:00',
/* author */ (''),
/* organization */ (''),
/* preprocessor_version */ 'ST-DEVELOPER v20.2',
/* originating_system */ 'Autodesk Translation Framework v15.17.0.0',
/* authorisation */ '');

FILE_SCHEMA (('AUTOMOTIVE_DESIGN { 1 0 10303 214 3 1 1 }'));
ENDSEC;

DATA;
#10=MECHANICAL_DESIGN_GEOMETRIC_PRESENTATION_REPRESENTATION('',(#958),#23728);
#738=SHAPE_REPRESENTATION_RELATIONSHIP('SRR','None',#24206,#844);
#844=ADVANCED_BREP_SHAPE_REPRESENTATION('',(#1071),#23706);
#958=STYLED_ITEM('',(#24779),#1071);
#1071=MANIFOLD_SOLID_BREP('Body1',#12489);
#1441=FACE_BOUND('',#3664,.T.);
#1442=FACE_BOUND('',#3666,.T.);
#1803=PLANE('',#15127);
#1804=PLANE('',#15128);
#2530=FACE_OUTER_BOUND('',#3661,.T.);
#2531=FACE_OUTER_BOUND('',#3662,.T.);
#2532=FACE_OUTER_BOUND('',#3663,.T.);
#2533=FACE_OUTER_BOUND('',#3665,.T.);
#3661=EDGE_LOOP('',(#10753,#10754,#10755,#10756));
#3662=EDGE_LOOP('',(#10757,#10758,#10759,#10760));
#3663=EDGE_LOOP('',(#10761));
#3664=EDGE_LOOP('',(#10762));
#3665=EDGE_LOOP('',(#10763));
#3666=EDGE_LOOP('',(#10764));
#4366=LINE('',#22819,#5041);
#4367=LINE('',#22825,#5042);
#5041=VECTOR('',#18885,0.225000000000001);
#5042=VECTOR('',#18892,1.);
#5858=CIRCLE('',#15122,0.225000000000001);
#5859=CIRCLE('',#15123,0.225000000000001);
#5860=CIRCLE('',#15125,1.);
#5861=CIRCLE('',#15126,1.);
#6757=VERTEX_POINT('',#22816);
#6758=VERTEX_POINT('',#22818);
#6759=VERTEX_POINT('',#22822);
#6760=VERTEX_POINT('',#22824);
#8116=EDGE_CURVE('',#6757,#6757,#5858,.T.);
#8117=EDGE_CURVE('',#6757,#6758,#4366,.T.);
#8118=EDGE_CURVE('',#6758,#6758,#5859,.T.);
#8119=EDGE_CURVE('',#6759,#6759,#5860,.T.);
#8120=EDGE_CURVE('',#6759,#6760,#4367,.T.);
#8121=EDGE_CURVE('',#6760,#6760,#5861,.T.);
#10753=ORIENTED_EDGE('',*,*,#8116,.F.);
#10754=ORIENTED_EDGE('',*,*,#8117,.T.);
#10755=ORIENTED_EDGE('',*,*,#8118,.T.);
#10756=ORIENTED_EDGE('',*,*,#8117,.F.);
#10757=ORIENTED_EDGE('',*,*,#8119,.F.);
#10758=ORIENTED_EDGE('',*,*,#8120,.T.);
#10759=ORIENTED_EDGE('',*,*,#8121,.T.);
#10760=ORIENTED_EDGE('',*,*,#8120,.F.);
#10761=ORIENTED_EDGE('',*,*,#8119,.T.);
#10762=ORIENTED_EDGE('',*,*,#8116,.T.);
#10763=ORIENTED_EDGE('',*,*,#8121,.F.);
#10764=ORIENTED_EDGE('',*,*,#8118,.F.);
#11572=CYLINDRICAL_SURFACE('',#15121,0.225000000000001);
#11573=CYLINDRICAL_SURFACE('',#15124,1.);
#12255=ADVANCED_FACE('',(#2530),#11572,.F.);
#12256=ADVANCED_FACE('',(#2531),#11573,.T.);
#12257=ADVANCED_FACE('',(#2532,#1441),#1803,.T.);
#12258=ADVANCED_FACE('',(#2533,#1442),#1804,.F.);
#12489=CLOSED_SHELL('',(#12255,#12256,#12257,#12258));
#15120=AXIS2_PLACEMENT_3D('',#22814,#18879,#18880);
#15121=AXIS2_PLACEMENT_3D('',#22815,#18881,#18882);
#15122=AXIS2_PLACEMENT_3D('',#22817,#18883,#18884);
#15123=AXIS2_PLACEMENT_3D('',#22820,#18886,#18887);
#15124=AXIS2_PLACEMENT_3D('',#22821,#18888,#18889);
#15125=AXIS2_PLACEMENT_3D('',#22823,#18890,#18891);
#15126=AXIS2_PLACEMENT_3D('',#22826,#18893,#18894);
#15127=AXIS2_PLACEMENT_3D('',#22827,#18895,#18896);
#15128=AXIS2_PLACEMENT_3D('',#22828,#18897,#18898);
#18879=DIRECTION('axis',(0.,0.,1.));
#18880=DIRECTION('refdir',(1.,0.,0.));
#18881=DIRECTION('center_axis',(0.,1.,0.));
#18882=DIRECTION('ref_axis',(1.,0.,0.));
#18883=DIRECTION('center_axis',(0.,-1.,0.));
#18884=DIRECTION('ref_axis',(1.,0.,0.));
#18885=DIRECTION('',(0.,-1.,0.));
#18886=DIRECTION('center_axis',(0.,-1.,0.));
#18887=DIRECTION('ref_axis',(1.,0.,0.));
#18888=DIRECTION('center_axis',(0.,1.,0.));
#18889=DIRECTION('ref_axis',(1.,0.,0.));
#18890=DIRECTION('center_axis',(0.,1.,0.));
#18891=DIRECTION('ref_axis',(1.,0.,0.));
#18892=DIRECTION('',(0.,-1.,0.));
#18893=DIRECTION('center_axis',(0.,1.,0.));
#18894=DIRECTION('ref_axis',(1.,0.,0.));
#18895=DIRECTION('center_axis',(0.,1.,0.));
#18896=DIRECTION('ref_axis',(1.,0.,0.));
#18897=DIRECTION('center_axis',(0.,1.,0.));
#18898=DIRECTION('ref_axis',(1.,0.,0.));
#22814=CARTESIAN_POINT('',(0.,0.,0.));
#22815=CARTESIAN_POINT('Origin',(24.2020784790221,-1.2,28.6577532024872));
#22816=CARTESIAN_POINT('',(23.9770784790221,-1.,28.6577532024872));
#22817=CARTESIAN_POINT('Origin',(24.2020784790221,-1.,28.6577532024872));
#22818=CARTESIAN_POINT('',(23.9770784790221,-1.2,28.6577532024872));
#22819=CARTESIAN_POINT('',(23.9770784790221,-1.2,28.6577532024872));
#22820=CARTESIAN_POINT('Origin',(24.2020784790221,-1.2,28.6577532024872));
#22821=CARTESIAN_POINT('Origin',(24.2020784790221,-1.2,28.6577532024872));
#22822=CARTESIAN_POINT('',(23.2020784790221,-1.,28.6577532024872));
#22823=CARTESIAN_POINT('Origin',(24.2020784790221,-1.,28.6577532024872));
#22824=CARTESIAN_POINT('',(23.2020784790221,-1.2,28.6577532024872));
#22825=CARTESIAN_POINT('',(23.2020784790221,-1.2,28.6577532024872));
#22826=CARTESIAN_POINT('Origin',(24.2020784790221,-1.2,28.6577532024872));
#22827=CARTESIAN_POINT('Origin',(24.2020784790221,-1.,28.6577532024872));
#22828=CARTESIAN_POINT('Origin',(24.2020784790221,-1.2,28.6577532024872));
#23589=UNCERTAINTY_MEASURE_WITH_UNIT(LENGTH_MEASURE(0.001),#23729,
'DISTANCE_ACCURACY_VALUE',
'Maximum model space distance between geometric entities at asserted c
onnectivities');
#23611=UNCERTAINTY_MEASURE_WITH_UNIT(LENGTH_MEASURE(0.001),#23729,
'DISTANCE_ACCURACY_VALUE',
'Maximum model space distance between geometric entities at asserted c
onnectivities');
#23706=(
GEOMETRIC_REPRESENTATION_CONTEXT(3)
GLOBAL_UNCERTAINTY_ASSIGNED_CONTEXT((#23589))
GLOBAL_UNIT_ASSIGNED_CONTEXT((#23729,#23731,#23732))
REPRESENTATION_CONTEXT('','3D')
);
#23728=(
GEOMETRIC_REPRESENTATION_CONTEXT(3)
GLOBAL_UNCERTAINTY_ASSIGNED_CONTEXT((#23611))
GLOBAL_UNIT_ASSIGNED_CONTEXT((#23729,#23731,#23732))
REPRESENTATION_CONTEXT('','3D')
);
#23729=(
LENGTH_UNIT()
NAMED_UNIT(*)
SI_UNIT(.CENTI.,.METRE.)
);
#23731=(
NAMED_UNIT(*)
PLANE_ANGLE_UNIT()
SI_UNIT($,.RADIAN.)
);
#23732=(
NAMED_UNIT(*)
SI_UNIT($,.STERADIAN.)
SOLID_ANGLE_UNIT()
);
#23827=SHAPE_DEFINITION_REPRESENTATION(#23994,#24206);
#23994=PRODUCT_DEFINITION_SHAPE('',$,#24323);
#24206=SHAPE_REPRESENTATION('',(#15120),#23706);
#24228=PRODUCT_DEFINITION_CONTEXT('part definition',#24578,'design');
#24323=PRODUCT_DEFINITION('Pivot keeper (3)','Pivot keeper (3)',#24439,#24228);
#24439=PRODUCT_DEFINITION_FORMATION('',$,#24674);
#24578=APPLICATION_CONTEXT(
'Core Data for Automotive Mechanical Design Process');
#24579=PRODUCT_CONTEXT('part definition',#24578,'mechanical');
#24674=PRODUCT('Pivot keeper (3)','Pivot keeper (3)','Pivot keeper (3)',(#24579));
#24773=COLOUR_RGB('Off White',0.89,0.88,0.83);
#24774=FILL_AREA_STYLE_COLOUR('',#24773);
#24775=FILL_AREA_STYLE('',(#24774));
#24776=SURFACE_STYLE_FILL_AREA(#24775);
#24777=SURFACE_SIDE_STYLE('',(#24776));
#24778=SURFACE_STYLE_USAGE(.BOTH.,#24777);
#24779=PRESENTATION_STYLE_ASSIGNMENT((#24778));
ENDSEC;
END-ISO-10303-21;
